ISO-10303-21;
HEADER;
/* Generated by software containing ST-Developer
 * from STEP Tools, Inc. (www.steptools.com) 
 */

FILE_DESCRIPTION(
/* description */ (''),
/* implementation_level */ '2;1');

FILE_NAME(
/* name */ 'ASME B18.16.6 Nylon Insert Lock Nut 6-32 UNC.step',
/* time_stamp */ '2026-10-15T13:29:10-07:00',
/* author */ (''),
/* organization */ (''),
/* preprocessor_version */ 'ST-DEVELOPER v20.2',
/* originating_system */ 'Autodesk Translation Framework v15.15.0.0',
/* authorisation */ '');

FILE_SCHEMA (('AUTOMOTIVE_DESIGN { 1 0 10303 214 3 1 1 }'));
ENDSEC;

DATA;
#10=MECHANICAL_DESIGN_GEOMETRIC_PRESENTATION_REPRESENTATION('',(#946),#83219);
#497=(
BOUNDED_CURVE()
B_SPLINE_CURVE(2,(#83095,#83096,#83097),.UNSPECIFIED.,.F.,.F.)
B_SPLINE_CURVE_WITH_KNOTS((3,3),(0.0765277474505289,0.571444001127736),
 .UNSPECIFIED.)
CURVE()
GEOMETRIC_REPRESENTATION_ITEM()
RATIONAL_B_SPLINE_CURVE((1.05846949482053,1.2222152955272,1.05846949482053))
REPRESENTATION_ITEM('')
);
#498=(
BOUNDED_CURVE()
B_SPLINE_CURVE(2,(#83099,#83100,#83101),.UNSPECIFIED.,.F.,.F.)
B_SPLINE_CURVE_WITH_KNOTS((3,3),(0.0765277474505272,0.571444001127737),
 .UNSPECIFIED.)
CURVE()
GEOMETRIC_REPRESENTATION_ITEM()
RATIONAL_B_SPLINE_CURVE((1.05846949482054,1.22221529552722,1.05846949482054))
REPRESENTATION_ITEM('')
);
#499=(
BOUNDED_CURVE()
B_SPLINE_CURVE(2,(#83103,#83104,#83105),.UNSPECIFIED.,.F.,.F.)
B_SPLINE_CURVE_WITH_KNOTS((3,3),(0.0765277474505292,0.571444001127744),
 .UNSPECIFIED.)
CURVE()
GEOMETRIC_REPRESENTATION_ITEM()
RATIONAL_B_SPLINE_CURVE((1.05846949482055,1.22221529552726,1.05846949482055))
REPRESENTATION_ITEM('')
);
#500=(
BOUNDED_CURVE()
B_SPLINE_CURVE(2,(#83107,#83108,#83109),.UNSPECIFIED.,.F.,.F.)
B_SPLINE_CURVE_WITH_KNOTS((3,3),(0.0765277474505268,0.571444001127737),
 .UNSPECIFIED.)
CURVE()
GEOMETRIC_REPRESENTATION_ITEM()
RATIONAL_B_SPLINE_CURVE((1.05846949482054,1.22221529552723,1.05846949482054))
REPRESENTATION_ITEM('')
);
#501=(
BOUNDED_CURVE()
B_SPLINE_CURVE(2,(#83111,#83112,#83113),.UNSPECIFIED.,.F.,.F.)
B_SPLINE_CURVE_WITH_KNOTS((3,3),(0.0765277474505273,0.571444001127738),
 .UNSPECIFIED.)
CURVE()
GEOMETRIC_REPRESENTATION_ITEM()
RATIONAL_B_SPLINE_CURVE((1.05846949482054,1.22221529552722,1.05846949482054))
REPRESENTATION_ITEM('')
);
#502=(
BOUNDED_CURVE()
B_SPLINE_CURVE(2,(#83114,#83115,#83116),.UNSPECIFIED.,.F.,.F.)
B_SPLINE_CURVE_WITH_KNOTS((3,3),(0.0765277474505272,0.571444001127742),
 .UNSPECIFIED.)
CURVE()
GEOMETRIC_REPRESENTATION_ITEM()
RATIONAL_B_SPLINE_CURVE((1.05846949482054,1.22221529552725,1.05846949482054))
REPRESENTATION_ITEM('')
);
#918=SHAPE_REPRESENTATION_RELATIONSHIP('SRR','None',#83313,#932);
#932=ADVANCED_BREP_SHAPE_REPRESENTATION('',(#960),#83218);
#946=STYLED_ITEM('',(#83392),#960);
#960=MANIFOLD_SOLID_BREP('Body1',#26942);
#1119=FACE_BOUND('',#5260,.T.);
#1120=FACE_BOUND('',#5264,.T.);
#1121=FACE_BOUND('',#5267,.T.);
#1122=FACE_BOUND('',#5276,.T.);
#2132=PLANE('',#29190);
#2133=PLANE('',#29197);
#2134=PLANE('',#29201);
#2135=PLANE('',#29203);
#2136=PLANE('',#29204);
#2137=PLANE('',#29205);
#2138=PLANE('',#29206);
#2139=PLANE('',#29207);
#2140=PLANE('',#29208);
#2141=PLANE('',#29209);
#2354=CYLINDRICAL_SURFACE('',#29188,1.80249999999999);
#2355=CYLINDRICAL_SURFACE('',#29192,3.59999999999999);
#2356=CYLINDRICAL_SURFACE('',#29199,1.9);
#3720=FACE_OUTER_BOUND('',#5257,.T.);
#3721=FACE_OUTER_BOUND('',#5258,.T.);
#3722=FACE_OUTER_BOUND('',#5259,.T.);
#3723=FACE_OUTER_BOUND('',#5261,.T.);
#3724=FACE_OUTER_BOUND('',#5262,.T.);
#3725=FACE_OUTER_BOUND('',#5263,.T.);
#3726=FACE_OUTER_BOUND('',#5265,.T.);
#3727=FACE_OUTER_BOUND('',#5266,.T.);
#3728=FACE_OUTER_BOUND('',#5268,.T.);
#3729=FACE_OUTER_BOUND('',#5269,.T.);
#3730=FACE_OUTER_BOUND('',#5270,.T.);
#3731=FACE_OUTER_BOUND('',#5271,.T.);
#3732=FACE_OUTER_BOUND('',#5272,.T.);
#3733=FACE_OUTER_BOUND('',#5273,.T.);
#3734=FACE_OUTER_BOUND('',#5274,.T.);
#3735=FACE_OUTER_BOUND('',#5275,.T.);
#5257=EDGE_LOOP('',(#25384,#25385,#25386,#25387));
#5258=EDGE_LOOP('',(#25388,#25389,#25390,#25391));
#5259=EDGE_LOOP('',(#25392));
#5260=EDGE_LOOP('',(#25393));
#5261=EDGE_LOOP('',(#25394,#25395,#25396,#25397));
#5262=EDGE_LOOP('',(#25398,#25399,#25400,#25401));
#5263=EDGE_LOOP('',(#25402));
#5264=EDGE_LOOP('',(#25403));
#5265=EDGE_LOOP('',(#25404,#25405,#25406,#25407));
#5266=EDGE_LOOP('',(#25408));
#5267=EDGE_LOOP('',(#25409));
#5268=EDGE_LOOP('',(#25410,#25411,#25412,#25413,#25414,#25415,#25416,#25417,
#25418));
#5269=EDGE_LOOP('',(#25419,#25420,#25421,#25422));
#5270=EDGE_LOOP('',(#25423,#25424,#25425,#25426));
#5271=EDGE_LOOP('',(#25427,#25428,#25429,#25430));
#5272=EDGE_LOOP('',(#25431,#25432,#25433,#25434));
#5273=EDGE_LOOP('',(#25435,#25436,#25437,#25438));
#5274=EDGE_LOOP('',(#25439,#25440,#25441,#25442));
#5275=EDGE_LOOP('',(#25443,#25444,#25445,#25446,#25447,#25448));
#5276=EDGE_LOOP('',(#25449));
#7770=LINE('',#83065,#10281);
#7771=LINE('',#83069,#10282);
#7772=LINE('',#83078,#10283);
#7773=LINE('',#83082,#10284);
#7774=LINE('',#83090,#10285);
#7775=LINE('',#83117,#10286);
#7776=LINE('',#83120,#10287);
#7777=LINE('',#83122,#10288);
#7778=LINE('',#83123,#10289);
#7779=LINE('',#83126,#10290);
#7780=LINE('',#83127,#10291);
#7781=LINE('',#83130,#10292);
#7782=LINE('',#83131,#10293);
#7783=LINE('',#83134,#10294);
#7784=LINE('',#83135,#10295);
#7785=LINE('',#83138,#10296);
#7786=LINE('',#83139,#10297);
#7787=LINE('',#83141,#10298);
#10281=VECTOR('',#35926,1.92749999999999);
#10282=VECTOR('',#35931,1.80249999999999);
#10283=VECTOR('',#35942,3.59999999999999);
#10284=VECTOR('',#35947,3.5);
#10285=VECTOR('',#35958,1.9);
#10286=VECTOR('',#35963,4.42651513084632);
#10287=VECTOR('',#35966,10.);
#10288=VECTOR('',#35967,10.);
#10289=VECTOR('',#35968,10.);
#10290=VECTOR('',#35971,10.);
#10291=VECTOR('',#35972,10.);
#10292=VECTOR('',#35975,10.);
#10293=VECTOR('',#35976,10.);
#10294=VECTOR('',#35979,10.);
#10295=VECTOR('',#35980,10.);
#10296=VECTOR('',#35983,10.);
#10297=VECTOR('',#35984,10.);
#10298=VECTOR('',#35987,10.);
#11042=CIRCLE('',#29186,1.80249999999999);
#11043=CIRCLE('',#29187,2.05249999999999);
#11044=CIRCLE('',#29189,1.80249999999999);
#11045=CIRCLE('',#29191,3.77031249999999);
#11046=CIRCLE('',#29193,3.59999999999999);
#11047=CIRCLE('',#29194,3.59999999999999);
#11048=CIRCLE('',#29196,3.4);
#11049=CIRCLE('',#29198,1.9);
#11050=CIRCLE('',#29200,1.9);
#13633=VERTEX_POINT('',#83062);
#13634=VERTEX_POINT('',#83064);
#13635=VERTEX_POINT('',#83068);
#13636=VERTEX_POINT('',#83072);
#13637=VERTEX_POINT('',#83075);
#13638=VERTEX_POINT('',#83077);
#13639=VERTEX_POINT('',#83081);
#13640=VERTEX_POINT('',#83085);
#13641=VERTEX_POINT('',#83088);
#13642=VERTEX_POINT('',#83093);
#13643=VERTEX_POINT('',#83094);
#13644=VERTEX_POINT('',#83098);
#13645=VERTEX_POINT('',#83102);
#13646=VERTEX_POINT('',#83106);
#13647=VERTEX_POINT('',#83110);
#13648=VERTEX_POINT('',#83119);
#13649=VERTEX_POINT('',#83121);
#13650=VERTEX_POINT('',#83125);
#13651=VERTEX_POINT('',#83129);
#13652=VERTEX_POINT('',#83133);
#13653=VERTEX_POINT('',#83137);
#17553=EDGE_CURVE('',#13633,#13633,#11042,.T.);
#17554=EDGE_CURVE('',#13633,#13634,#7770,.T.);
#17555=EDGE_CURVE('',#13634,#13634,#11043,.T.);
#17556=EDGE_CURVE('',#13633,#13635,#7771,.T.);
#17557=EDGE_CURVE('',#13635,#13635,#11044,.T.);
#17558=EDGE_CURVE('',#13636,#13636,#11045,.T.);
#17559=EDGE_CURVE('',#13637,#13637,#11046,.T.);
#17560=EDGE_CURVE('',#13637,#13638,#7772,.T.);
#17561=EDGE_CURVE('',#13638,#13638,#11047,.T.);
#17562=EDGE_CURVE('',#13637,#13639,#7773,.T.);
#17563=EDGE_CURVE('',#13639,#13639,#11048,.T.);
#17564=EDGE_CURVE('',#13640,#13640,#11049,.T.);
#17565=EDGE_CURVE('',#13641,#13641,#11050,.T.);
#17566=EDGE_CURVE('',#13641,#13640,#7774,.T.);
#17567=EDGE_CURVE('',#13642,#13643,#497,.T.);
#17568=EDGE_CURVE('',#13644,#13642,#498,.T.);
#17569=EDGE_CURVE('',#13645,#13644,#499,.T.);
#17570=EDGE_CURVE('',#13646,#13645,#500,.T.);
#17571=EDGE_CURVE('',#13647,#13646,#501,.T.);
#17572=EDGE_CURVE('',#13643,#13647,#502,.T.);
#17573=EDGE_CURVE('',#13643,#13636,#7775,.T.);
#17574=EDGE_CURVE('',#13648,#13643,#7776,.T.);
#17575=EDGE_CURVE('',#13649,#13648,#7777,.T.);
#17576=EDGE_CURVE('',#13649,#13642,#7778,.T.);
#17577=EDGE_CURVE('',#13650,#13647,#7779,.T.);
#17578=EDGE_CURVE('',#13648,#13650,#7780,.T.);
#17579=EDGE_CURVE('',#13651,#13646,#7781,.T.);
#17580=EDGE_CURVE('',#13650,#13651,#7782,.T.);
#17581=EDGE_CURVE('',#13652,#13645,#7783,.T.);
#17582=EDGE_CURVE('',#13651,#13652,#7784,.T.);
#17583=EDGE_CURVE('',#13653,#13644,#7785,.T.);
#17584=EDGE_CURVE('',#13652,#13653,#7786,.T.);
#17585=EDGE_CURVE('',#13653,#13649,#7787,.T.);
#25384=ORIENTED_EDGE('',*,*,#17553,.T.);
#25385=ORIENTED_EDGE('',*,*,#17554,.T.);
#25386=ORIENTED_EDGE('',*,*,#17555,.T.);
#25387=ORIENTED_EDGE('',*,*,#17554,.F.);
#25388=ORIENTED_EDGE('',*,*,#17553,.F.);
#25389=ORIENTED_EDGE('',*,*,#17556,.T.);
#25390=ORIENTED_EDGE('',*,*,#17557,.F.);
#25391=ORIENTED_EDGE('',*,*,#17556,.F.);
#25392=ORIENTED_EDGE('',*,*,#17558,.T.);
#25393=ORIENTED_EDGE('',*,*,#17555,.F.);
#25394=ORIENTED_EDGE('',*,*,#17559,.F.);
#25395=ORIENTED_EDGE('',*,*,#17560,.T.);
#25396=ORIENTED_EDGE('',*,*,#17561,.F.);
#25397=ORIENTED_EDGE('',*,*,#17560,.F.);
#25398=ORIENTED_EDGE('',*,*,#17559,.T.);
#25399=ORIENTED_EDGE('',*,*,#17562,.T.);
#25400=ORIENTED_EDGE('',*,*,#17563,.F.);
#25401=ORIENTED_EDGE('',*,*,#17562,.F.);
#25402=ORIENTED_EDGE('',*,*,#17563,.T.);
#25403=ORIENTED_EDGE('',*,*,#17564,.F.);
#25404=ORIENTED_EDGE('',*,*,#17565,.F.);
#25405=ORIENTED_EDGE('',*,*,#17566,.T.);
#25406=ORIENTED_EDGE('',*,*,#17564,.T.);
#25407=ORIENTED_EDGE('',*,*,#17566,.F.);
#25408=ORIENTED_EDGE('',*,*,#17565,.T.);
#25409=ORIENTED_EDGE('',*,*,#17557,.T.);
#25410=ORIENTED_EDGE('',*,*,#17567,.F.);
#25411=ORIENTED_EDGE('',*,*,#17568,.F.);
#25412=ORIENTED_EDGE('',*,*,#17569,.F.);
#25413=ORIENTED_EDGE('',*,*,#17570,.F.);
#25414=ORIENTED_EDGE('',*,*,#17571,.F.);
#25415=ORIENTED_EDGE('',*,*,#17572,.F.);
#25416=ORIENTED_EDGE('',*,*,#17573,.T.);
#25417=ORIENTED_EDGE('',*,*,#17558,.F.);
#25418=ORIENTED_EDGE('',*,*,#17573,.F.);
#25419=ORIENTED_EDGE('',*,*,#17567,.T.);
#25420=ORIENTED_EDGE('',*,*,#17574,.F.);
#25421=ORIENTED_EDGE('',*,*,#17575,.F.);
#25422=ORIENTED_EDGE('',*,*,#17576,.T.);
#25423=ORIENTED_EDGE('',*,*,#17572,.T.);
#25424=ORIENTED_EDGE('',*,*,#17577,.F.);
#25425=ORIENTED_EDGE('',*,*,#17578,.F.);
#25426=ORIENTED_EDGE('',*,*,#17574,.T.);
#25427=ORIENTED_EDGE('',*,*,#17571,.T.);
#25428=ORIENTED_EDGE('',*,*,#17579,.F.);
#25429=ORIENTED_EDGE('',*,*,#17580,.F.);
#25430=ORIENTED_EDGE('',*,*,#17577,.T.);
#25431=ORIENTED_EDGE('',*,*,#17570,.T.);
#25432=ORIENTED_EDGE('',*,*,#17581,.F.);
#25433=ORIENTED_EDGE('',*,*,#17582,.F.);
#25434=ORIENTED_EDGE('',*,*,#17579,.T.);
#25435=ORIENTED_EDGE('',*,*,#17569,.T.);
#25436=ORIENTED_EDGE('',*,*,#17583,.F.);
#25437=ORIENTED_EDGE('',*,*,#17584,.F.);
#25438=ORIENTED_EDGE('',*,*,#17581,.T.);
#25439=ORIENTED_EDGE('',*,*,#17568,.T.);
#25440=ORIENTED_EDGE('',*,*,#17576,.F.);
#25441=ORIENTED_EDGE('',*,*,#17585,.F.);
#25442=ORIENTED_EDGE('',*,*,#17583,.T.);
#25443=ORIENTED_EDGE('',*,*,#17580,.T.);
#25444=ORIENTED_EDGE('',*,*,#17582,.T.);
#25445=ORIENTED_EDGE('',*,*,#17584,.T.);
#25446=ORIENTED_EDGE('',*,*,#17585,.T.);
#25447=ORIENTED_EDGE('',*,*,#17575,.T.);
#25448=ORIENTED_EDGE('',*,*,#17578,.T.);
#25449=ORIENTED_EDGE('',*,*,#17561,.T.);
#25547=CONICAL_SURFACE('',#29185,1.92749999999999,0.785398163397448);
#25548=CONICAL_SURFACE('',#29195,3.5,0.785398163397426);
#25549=CONICAL_SURFACE('',#29202,4.42651513084632,1.04719755119659);
#26913=ADVANCED_FACE('',(#3720),#25547,.F.);
#26914=ADVANCED_FACE('',(#3721),#2354,.F.);
#26915=ADVANCED_FACE('',(#3722,#1119),#2132,.T.);
#26916=ADVANCED_FACE('',(#3723),#2355,.T.);
#26917=ADVANCED_FACE('',(#3724),#25548,.T.);
#26918=ADVANCED_FACE('',(#3725,#1120),#2133,.T.);
#26919=ADVANCED_FACE('',(#3726),#2356,.F.);
#26920=ADVANCED_FACE('',(#3727,#1121),#2134,.F.);
#26921=ADVANCED_FACE('',(#3728),#25549,.T.);
#26922=ADVANCED_FACE('',(#3729),#2135,.T.);
#26923=ADVANCED_FACE('',(#3730),#2136,.T.);
#26924=ADVANCED_FACE('',(#3731),#2137,.T.);
#26925=ADVANCED_FACE('',(#3732),#2138,.T.);
#26926=ADVANCED_FACE('',(#3733),#2139,.T.);
#26927=ADVANCED_FACE('',(#3734),#2140,.T.);
#26928=ADVANCED_FACE('',(#3735,#1122),#2141,.F.);
#26942=CLOSED_SHELL('',(#26913,#26914,#26915,#26916,#26917,#26918,#26919,
#26920,#26921,#26922,#26923,#26924,#26925,#26926,#26927,#26928));
#29184=AXIS2_PLACEMENT_3D('',#83060,#35920,#35921);
#29185=AXIS2_PLACEMENT_3D('',#83061,#35922,#35923);
#29186=AXIS2_PLACEMENT_3D('',#83063,#35924,#35925);
#29187=AXIS2_PLACEMENT_3D('',#83066,#35927,#35928);
#29188=AXIS2_PLACEMENT_3D('',#83067,#35929,#35930);
#29189=AXIS2_PLACEMENT_3D('',#83070,#35932,#35933);
#29190=AXIS2_PLACEMENT_3D('',#83071,#35934,#35935);
#29191=AXIS2_PLACEMENT_3D('',#83073,#35936,#35937);
#29192=AXIS2_PLACEMENT_3D('',#83074,#35938,#35939);
#29193=AXIS2_PLACEMENT_3D('',#83076,#35940,#35941);
#29194=AXIS2_PLACEMENT_3D('',#83079,#35943,#35944);
#29195=AXIS2_PLACEMENT_3D('',#83080,#35945,#35946);
#29196=AXIS2_PLACEMENT_3D('',#83083,#35948,#35949);
#29197=AXIS2_PLACEMENT_3D('',#83084,#35950,#35951);
#29198=AXIS2_PLACEMENT_3D('',#83086,#35952,#35953);
#29199=AXIS2_PLACEMENT_3D('',#83087,#35954,#35955);
#29200=AXIS2_PLACEMENT_3D('',#83089,#35956,#35957);
#29201=AXIS2_PLACEMENT_3D('',#83091,#35959,#35960);
#29202=AXIS2_PLACEMENT_3D('',#83092,#35961,#35962);
#29203=AXIS2_PLACEMENT_3D('',#83118,#35964,#35965);
#29204=AXIS2_PLACEMENT_3D('',#83124,#35969,#35970);
#29205=AXIS2_PLACEMENT_3D('',#83128,#35973,#35974);
#29206=AXIS2_PLACEMENT_3D('',#83132,#35977,#35978);
#29207=AXIS2_PLACEMENT_3D('',#83136,#35981,#35982);
#29208=AXIS2_PLACEMENT_3D('',#83140,#35985,#35986);
#29209=AXIS2_PLACEMENT_3D('',#83142,#35988,#35989);
#35920=DIRECTION('axis',(0.,0.,1.));
#35921=DIRECTION('refdir',(1.,0.,0.));
#35922=DIRECTION('center_axis',(0.,1.,0.));
#35923=DIRECTION('ref_axis',(1.,0.,0.));
#35924=DIRECTION('center_axis',(0.,-1.,0.));
#35925=DIRECTION('ref_axis',(1.,0.,0.));
#35926=DIRECTION('',(-0.707106781186547,0.707106781186548,8.65956056235493E-17));
#35927=DIRECTION('center_axis',(0.,1.,0.));
#35928=DIRECTION('ref_axis',(1.,0.,0.));
#35929=DIRECTION('center_axis',(0.,-1.,0.));
#35930=DIRECTION('ref_axis',(1.,0.,0.));
#35931=DIRECTION('',(0.,-1.,0.));
#35932=DIRECTION('center_axis',(0.,1.,0.));
#35933=DIRECTION('ref_axis',(1.,0.,0.));
#35934=DIRECTION('center_axis',(0.,1.,0.));
#35935=DIRECTION('ref_axis',(0.,0.,1.));
#35936=DIRECTION('center_axis',(0.,1.,0.));
#35937=DIRECTION('ref_axis',(1.,0.,0.));
#35938=DIRECTION('center_axis',(0.,-1.,0.));
#35939=DIRECTION('ref_axis',(1.,0.,0.));
#35940=DIRECTION('center_axis',(0.,-1.,0.));
#35941=DIRECTION('ref_axis',(1.,0.,0.));
#35942=DIRECTION('',(0.,1.,0.));
#35943=DIRECTION('center_axis',(0.,1.,0.));
#35944=DIRECTION('ref_axis',(1.,0.,0.));
#35945=DIRECTION('center_axis',(0.,1.,0.));
#35946=DIRECTION('ref_axis',(1.,0.,0.));
#35947=DIRECTION('',(0.707106781186532,-0.707106781186563,-8.65956056235474E-17));
#35948=DIRECTION('center_axis',(0.,-1.,0.));
#35949=DIRECTION('ref_axis',(1.,0.,0.));
#35950=DIRECTION('center_axis',(0.,-1.,0.));
#35951=DIRECTION('ref_axis',(0.,0.,-1.));
#35952=DIRECTION('center_axis',(0.,-1.,0.));
#35953=DIRECTION('ref_axis',(1.,0.,0.));
#35954=DIRECTION('center_axis',(0.,-1.,0.));
#35955=DIRECTION('ref_axis',(1.,0.,0.));
#35956=DIRECTION('center_axis',(0.,-1.,0.));
#35957=DIRECTION('ref_axis',(1.,0.,0.));
#35958=DIRECTION('',(0.,-1.,0.));
#35959=DIRECTION('center_axis',(0.,1.,0.));
#35960=DIRECTION('ref_axis',(1.,0.,0.));
#35961=DIRECTION('center_axis',(0.,-1.,0.));
#35962=DIRECTION('ref_axis',(1.,0.,0.));
#35963=DIRECTION('',(0.866025403784435,0.500000000000007,1.0605752387249E-16));
#35964=DIRECTION('center_axis',(-0.866025403784439,0.,0.5));
#35965=DIRECTION('ref_axis',(0.5,0.,0.866025403784439));
#35966=DIRECTION('',(0.,1.,0.));
#35967=DIRECTION('',(-0.5,0.,-0.866025403784439));
#35968=DIRECTION('',(0.,1.,0.));
#35969=DIRECTION('center_axis',(-0.866025403784439,0.,-0.5));
#35970=DIRECTION('ref_axis',(-0.5,0.,0.866025403784439));
#35971=DIRECTION('',(0.,1.,0.));
#35972=DIRECTION('',(0.5,0.,-0.866025403784438));
#35973=DIRECTION('center_axis',(-2.42263015607378E-16,0.,-1.));
#35974=DIRECTION('ref_axis',(-1.,0.,2.42263015607378E-16));
#35975=DIRECTION('',(0.,1.,0.));
#35976=DIRECTION('',(1.,0.,-2.42263015607378E-16));
#35977=DIRECTION('center_axis',(0.86602540378444,0.,-0.499999999999997));
#35978=DIRECTION('ref_axis',(-0.499999999999997,0.,-0.86602540378444));
#35979=DIRECTION('',(0.,1.,0.));
#35980=DIRECTION('',(0.499999999999997,0.,0.86602540378444));
#35981=DIRECTION('center_axis',(0.86602540378444,0.,0.499999999999997));
#35982=DIRECTION('ref_axis',(0.499999999999997,0.,-0.86602540378444));
#35983=DIRECTION('',(0.,1.,0.));
#35984=DIRECTION('',(-0.499999999999997,0.,0.86602540378444));
#35985=DIRECTION('center_axis',(0.,0.,1.));
#35986=DIRECTION('ref_axis',(1.,0.,0.));
#35987=DIRECTION('',(-1.,0.,0.));
#35988=DIRECTION('center_axis',(0.,1.,0.));
#35989=DIRECTION('ref_axis',(1.,0.,0.));
#83060=CARTESIAN_POINT('',(0.,0.,0.));
#83061=CARTESIAN_POINT('Origin',(88.011,52.9504,12.066));
#83062=CARTESIAN_POINT('',(86.2085,52.8254,12.066));
#83063=CARTESIAN_POINT('Origin',(88.011,52.8254,12.066));
#83064=CARTESIAN_POINT('',(85.9585,53.0754,12.066));
#83065=CARTESIAN_POINT('',(86.0835,52.9504,12.066));
#83066=CARTESIAN_POINT('Origin',(88.011,53.0754,12.066));
#83067=CARTESIAN_POINT('Origin',(88.011,53.0754,12.066));
#83068=CARTESIAN_POINT('',(86.2085,50.1254,12.066));
#83069=CARTESIAN_POINT('',(86.2085,53.0754,12.066));
#83070=CARTESIAN_POINT('Origin',(88.011,50.1254,12.066));
#83071=CARTESIAN_POINT('Origin',(88.011,53.0754,12.066));
#83072=CARTESIAN_POINT('',(84.2406875,53.0754,12.066));
#83073=CARTESIAN_POINT('Origin',(88.011,53.0754,12.066));
#83074=CARTESIAN_POINT('Origin',(88.011,49.516,12.066));
#83075=CARTESIAN_POINT('',(84.411,48.9066,12.066));
#83076=CARTESIAN_POINT('Origin',(88.011,48.9066,12.066));
#83077=CARTESIAN_POINT('',(84.411,50.1254,12.066));
#83078=CARTESIAN_POINT('',(84.411,49.516,12.066));
#83079=CARTESIAN_POINT('Origin',(88.011,50.1254,12.066));
#83080=CARTESIAN_POINT('Origin',(88.011,48.8066,12.066));
#83081=CARTESIAN_POINT('',(84.611,48.7066,12.066));
#83082=CARTESIAN_POINT('',(84.511,48.8066,12.066));
#83083=CARTESIAN_POINT('Origin',(88.011,48.7066,12.066));
#83084=CARTESIAN_POINT('Origin',(89.911,48.7066,12.066));
#83085=CARTESIAN_POINT('',(86.111,48.7066,12.066));
#83086=CARTESIAN_POINT('Origin',(88.011,48.7066,12.066));
#83087=CARTESIAN_POINT('Origin',(88.011,49.416,12.066));
#83088=CARTESIAN_POINT('',(86.111,50.1254,12.066));
#83089=CARTESIAN_POINT('Origin',(88.011,50.1254,12.066));
#83090=CARTESIAN_POINT('',(86.111,49.416,12.066));
#83091=CARTESIAN_POINT('Origin',(88.011,50.1254,12.066));
#83092=CARTESIAN_POINT('Origin',(88.011,52.6965412344379,12.066));
#83093=CARTESIAN_POINT('',(85.7196411191537,52.6063576034707,16.03475));
#83094=CARTESIAN_POINT('',(83.4282822383073,52.6063576034707,12.066));
#83095=CARTESIAN_POINT('Ctrl Pts',(85.7196411191537,52.6063576034707,16.03475));
#83096=CARTESIAN_POINT('Ctrl Pts',(84.5739616787304,53.2678159368036,14.0503749999999));
#83097=CARTESIAN_POINT('Ctrl Pts',(83.4282822383073,52.6063576034707,12.066));
#83098=CARTESIAN_POINT('',(90.3023588808463,52.6063576034707,16.03475));
#83099=CARTESIAN_POINT('Ctrl Pts',(90.3023588808463,52.6063576034707,16.03475));
#83100=CARTESIAN_POINT('Ctrl Pts',(88.0109999999998,53.2678159368036,16.03475));
#83101=CARTESIAN_POINT('Ctrl Pts',(85.7196411191537,52.6063576034707,16.03475));
#83102=CARTESIAN_POINT('',(92.5937177616926,52.6063576034707,12.066));
#83103=CARTESIAN_POINT('Ctrl Pts',(92.5937177616926,52.6063576034707,12.066));
#83104=CARTESIAN_POINT('Ctrl Pts',(91.4480383212694,53.2678159368036,14.0503750000001));
#83105=CARTESIAN_POINT('Ctrl Pts',(90.3023588808463,52.6063576034707,16.03475));
#83106=CARTESIAN_POINT('',(90.3023588808463,52.6063576034707,8.09725));
#83107=CARTESIAN_POINT('Ctrl Pts',(90.3023588808463,52.6063576034707,8.09725));
#83108=CARTESIAN_POINT('Ctrl Pts',(91.4480383212696,53.2678159368036,10.0816250000001));
#83109=CARTESIAN_POINT('Ctrl Pts',(92.5937177616926,52.6063576034707,12.066));
#83110=CARTESIAN_POINT('',(85.7196411191537,52.6063576034707,8.09725));
#83111=CARTESIAN_POINT('Ctrl Pts',(85.7196411191537,52.6063576034707,8.09725));
#83112=CARTESIAN_POINT('Ctrl Pts',(88.0110000000002,53.2678159368036,8.09725));
#83113=CARTESIAN_POINT('Ctrl Pts',(90.3023588808463,52.6063576034707,8.09725));
#83114=CARTESIAN_POINT('Ctrl Pts',(83.4282822383073,52.6063576034707,12.066));
#83115=CARTESIAN_POINT('Ctrl Pts',(84.5739616787306,53.2678159368036,10.0816249999999));
#83116=CARTESIAN_POINT('Ctrl Pts',(85.7196411191537,52.6063576034707,8.09725000000001));
#83117=CARTESIAN_POINT('',(83.5844848691537,52.6965412344379,12.066));
#83118=CARTESIAN_POINT('Origin',(83.4282822383073,50.1254,12.066));
#83119=CARTESIAN_POINT('',(83.4282822383073,50.1254,12.066));
#83120=CARTESIAN_POINT('',(83.4282822383073,50.1254,12.066));
#83121=CARTESIAN_POINT('',(85.7196411191537,50.1254,16.03475));
#83122=CARTESIAN_POINT('',(85.7196411191537,50.1254,16.03475));
#83123=CARTESIAN_POINT('',(85.7196411191537,50.1254,16.03475));
#83124=CARTESIAN_POINT('Origin',(85.7196411191537,50.1254,8.09725));
#83125=CARTESIAN_POINT('',(85.7196411191537,50.1254,8.09725));
#83126=CARTESIAN_POINT('',(85.7196411191537,50.1254,8.09725));
#83127=CARTESIAN_POINT('',(83.4282822383073,50.1254,12.066));
#83128=CARTESIAN_POINT('Origin',(90.3023588808463,50.1254,8.09725));
#83129=CARTESIAN_POINT('',(90.3023588808463,50.1254,8.09725));
#83130=CARTESIAN_POINT('',(90.3023588808463,50.1254,8.09725));
#83131=CARTESIAN_POINT('',(85.7196411191537,50.1254,8.09725));
#83132=CARTESIAN_POINT('Origin',(92.5937177616926,50.1254,12.066));
#83133=CARTESIAN_POINT('',(92.5937177616926,50.1254,12.066));
#83134=CARTESIAN_POINT('',(92.5937177616926,50.1254,12.066));
#83135=CARTESIAN_POINT('',(90.3023588808463,50.1254,8.09725));
#83136=CARTESIAN_POINT('Origin',(90.3023588808463,50.1254,16.03475));
#83137=CARTESIAN_POINT('',(90.3023588808463,50.1254,16.03475));
#83138=CARTESIAN_POINT('',(90.3023588808463,50.1254,16.03475));
#83139=CARTESIAN_POINT('',(92.5937177616926,50.1254,12.066));
#83140=CARTESIAN_POINT('Origin',(85.7196411191537,50.1254,16.03475));
#83141=CARTESIAN_POINT('',(90.3023588808463,50.1254,16.03475));
#83142=CARTESIAN_POINT('Origin',(88.011,50.1254,12.066));
#83202=UNCERTAINTY_MEASURE_WITH_UNIT(LENGTH_MEASURE(0.01),#83220,
'DISTANCE_ACCURACY_VALUE',
'Maximum model space distance between geometric entities at asserted c
onnectivities');
#83203=UNCERTAINTY_MEASURE_WITH_UNIT(LENGTH_MEASURE(0.01),#83220,
'DISTANCE_ACCURACY_VALUE',
'Maximum model space distance between geometric entities at asserted c
onnectivities');
#83218=(
GEOMETRIC_REPRESENTATION_CONTEXT(3)
GLOBAL_UNCERTAINTY_ASSIGNED_CONTEXT((#83202))
GLOBAL_UNIT_ASSIGNED_CONTEXT((#83220,#83222,#83223))
REPRESENTATION_CONTEXT('','3D')
);
#83219=(
GEOMETRIC_REPRESENTATION_CONTEXT(3)
GLOBAL_UNCERTAINTY_ASSIGNED_CONTEXT((#83203))
GLOBAL_UNIT_ASSIGNED_CONTEXT((#83220,#83222,#83223))
REPRESENTATION_CONTEXT('','3D')
);
#83220=(
LENGTH_UNIT()
NAMED_UNIT(*)
SI_UNIT(.MILLI.,.METRE.)
);
#83222=(
NAMED_UNIT(*)
PLANE_ANGLE_UNIT()
SI_UNIT($,.RADIAN.)
);
#83223=(
NAMED_UNIT(*)
SI_UNIT($,.STERADIAN.)
SOLID_ANGLE_UNIT()
);
#83238=SHAPE_DEFINITION_REPRESENTATION(#83253,#83313);
#83253=PRODUCT_DEFINITION_SHAPE('',$,#83329);
#83313=SHAPE_REPRESENTATION('',(#29184),#83218);
#83314=PRODUCT_DEFINITION_CONTEXT('part definition',#83361,'design');
#83329=PRODUCT_DEFINITION(
'ASME B18.16.6 Nylon Insert Lock Nut 6-32 UNC',
'ASME B18.16.6 Nylon Insert Lock Nut 6-32 UNC',#83344,#83314);
#83344=PRODUCT_DEFINITION_FORMATION('',$,#83377);
#83361=APPLICATION_CONTEXT(
'Core Data for Automotive Mechanical Design Process');
#83362=PRODUCT_CONTEXT('part definition',#83361,'mechanical');
#83377=PRODUCT('ASME B18.16.6 Nylon Insert Lock Nut 6-32 UNC',
'ASME B18.16.6 Nylon Insert Lock Nut 6-32 UNC',$,(#83362));
#83392=PRESENTATION_STYLE_ASSIGNMENT((#83407));
#83407=SURFACE_STYLE_USAGE(.BOTH.,#83422);
#83422=SURFACE_SIDE_STYLE('',(#83437));
#83437=SURFACE_STYLE_FILL_AREA(#83452);
#83452=FILL_AREA_STYLE('Opaque(203,207,213)',(#83467));
#83467=FILL_AREA_STYLE_COLOUR('Opaque(203,207,213)',#83482);
#83482=COLOUR_RGB('Opaque(203,207,213)', 0.31764706, 0.68627451, 0.89019608);
ENDSEC;
END-ISO-10303-21;
